ISO-10303-21;
HEADER;
/* Generated by software containing ST-Developer
 * from STEP Tools, Inc. (www.steptools.com) 
 */
/* OPTION: using custom renumber hook */

FILE_DESCRIPTION(
/* description */ ('STEP AP242 Edition 2', 'CAx-IF Rec.Pracs.---Representation and Presentation of Product Manufa
cturing Information (PMI)---4.0---2014-10-13', 'CAx-IF Rec.Pracs.---3D Tessellated Geometry---0.4---2014-09-14', '2;1', 'CAx-IF Rec.Pracs.---User Defined Attributes---1.5---2016-08-15'),
/* implementation_level */ '2;1');

FILE_NAME(
/* name */ 'ball_outlet_valve.step',
/* time_stamp */ '2026-10-08T12:15:07Z',
/* author */ (''),
/* organization */ (''),
/* preprocessor_version */ 'ST-DEVELOPER v20',
/* originating_system */ 'ONSHAPE BY PTC INC, 1.221',
/* authorisation */ '  ');

FILE_SCHEMA (('AP242_MANAGED_MODEL_BASED_3D_ENGINEERING_MIM_LF { 1 0 10303 442 3 1 4 }'));
ENDSEC;

DATA;
#12=VERTEX_LOOP('',#8212);
#16=SPHERICAL_SURFACE('',#14697,0.0015);
#60=COLOUR_RGB('', 0.66274510, 0.83137255, 0.94901961);
#216=SHAPE_REPRESENTATION_RELATIONSHIP('','',#13790,#243);
#243=ADVANCED_BREP_SHAPE_REPRESENTATION('',(#13734),#45480);
#8212=VERTEX_POINT('',#35048);
#12209=FACE_BOUND('',#12,.T.);
#13182=ADVANCED_FACE('',(#12209),#16,.T.);
#13517=CLOSED_SHELL('',(#13182));
#13544=STYLED_ITEM('',(#13571),#13734);
#13571=PRESENTATION_STYLE_ASSIGNMENT((#13598));
#13598=SURFACE_STYLE_USAGE(.BOTH.,#13625);
#13625=SURFACE_SIDE_STYLE('',(#13652));
#13652=SURFACE_STYLE_FILL_AREA(#13679);
#13679=FILL_AREA_STYLE('',(#13706));
#13706=FILL_AREA_STYLE_COLOUR('',#60);
#13734=MANIFOLD_SOLID_BREP('ball_outlet_valve',#13517);
#13762=SHAPE_DEFINITION_REPRESENTATION(#45557,#13790);
#13790=SHAPE_REPRESENTATION('ball_outlet_valve',(#13802),#45480);
#13802=AXIS2_PLACEMENT_3D('',#19109,#15295,#15296);
#14697=AXIS2_PLACEMENT_3D('',#35047,#17567,#17568);
#15295=DIRECTION('',(0.,0.,1.));
#15296=DIRECTION('',(1.,0.,0.));
#17567=DIRECTION('',(0.,-1.,0.));
#17568=DIRECTION('',(1.,0.,0.));
#19109=CARTESIAN_POINT('',(0.,0.,0.));
#35047=CARTESIAN_POINT('',(0.,0.,0.));
#35048=CARTESIAN_POINT('',(9.18485099360515E-20,0.0015,0.));
#45463=MECHANICAL_DESIGN_GEOMETRIC_PRESENTATION_REPRESENTATION('',(#13544),#45464);
#45464=(
GEOMETRIC_REPRESENTATION_CONTEXT(3)
GLOBAL_UNCERTAINTY_ASSIGNED_CONTEXT((#45492))
GLOBAL_UNIT_ASSIGNED_CONTEXT((#45522,#45521,#45520))
REPRESENTATION_CONTEXT('MAS-690','TOP_LEVEL_ASSEMBLY_PART')
);
#45480=(
GEOMETRIC_REPRESENTATION_CONTEXT(3)
GLOBAL_UNCERTAINTY_ASSIGNED_CONTEXT((#45508))
GLOBAL_UNIT_ASSIGNED_CONTEXT((#45522,#45521,#45520))
REPRESENTATION_CONTEXT('ball_outlet_valve','COMPONENT_PART')
);
#45492=UNCERTAINTY_MEASURE_WITH_UNIT(LENGTH_MEASURE(1.E-8),#45522,
'DISTANCE_ACCURACY_VALUE','Maximum Tolerance applied to model');
#45508=UNCERTAINTY_MEASURE_WITH_UNIT(LENGTH_MEASURE(1.E-8),#45522,
'DISTANCE_ACCURACY_VALUE','Maximum Tolerance applied to model');
#45520=(
NAMED_UNIT(*)
SI_UNIT($,.STERADIAN.)
SOLID_ANGLE_UNIT()
);
#45521=(
NAMED_UNIT(*)
PLANE_ANGLE_UNIT()
SI_UNIT($,.RADIAN.)
);
#45522=(
LENGTH_UNIT()
NAMED_UNIT(*)
SI_UNIT($,.METRE.)
);
#45557=PRODUCT_DEFINITION_SHAPE('','',#45601);
#45601=PRODUCT_DEFINITION('','',#45657,#45629);
#45629=PRODUCT_DEFINITION_CONTEXT('',#45782,'design');
#45657=PRODUCT_DEFINITION_FORMATION_WITH_SPECIFIED_SOURCE('','',#45713,
 .NOT_KNOWN.);
#45713=PRODUCT('ball_outlet_valve','ball_outlet_valve',
'ball_outlet_valve',(#45769));
#45769=PRODUCT_CONTEXT('',#45782,'mechanical');
#45782=APPLICATION_CONTEXT('managed model based 3d engineering');
ENDSEC;
END-ISO-10303-21;
